ISO-10303-21;
HEADER;
/* Generated by software containing ST-Developer
 * from STEP Tools, Inc. (www.steptools.com) 
 */

FILE_DESCRIPTION(
/* description */ ('PAT-041'),
/* implementation_level */ '2;1');

FILE_NAME(
/* name */ 'Weld-on flange (1).step',
/* time_stamp */ '2026-10-28T22:21:24-07:00',
/* author */ (''),
/* organization */ (''),
/* preprocessor_version */ 'ST-DEVELOPER v20.2',
/* originating_system */ 'Autodesk Translation Framework v15.17.0.0',
/* authorisation */ '');

FILE_SCHEMA (('AUTOMOTIVE_DESIGN { 1 0 10303 214 3 1 1 }'));
ENDSEC;

DATA;
#10=MECHANICAL_DESIGN_GEOMETRIC_PRESENTATION_REPRESENTATION('',(#211),#2507);
#191=SHAPE_REPRESENTATION_RELATIONSHIP('SRR','None',#2576,#201);
#201=ADVANCED_BREP_SHAPE_REPRESENTATION('',(#221),#2499);
#211=STYLED_ITEM('',(#2687),#221);
#221=MANIFOLD_SOLID_BREP('Body1',#1331);
#241=FACE_BOUND('',#415,.T.);
#242=FACE_BOUND('',#416,.T.);
#243=FACE_BOUND('',#417,.T.);
#244=FACE_BOUND('',#418,.T.);
#245=FACE_BOUND('',#419,.T.);
#246=FACE_BOUND('',#421,.T.);
#247=FACE_BOUND('',#422,.T.);
#248=FACE_BOUND('',#423,.T.);
#249=FACE_BOUND('',#424,.T.);
#250=FACE_BOUND('',#425,.T.);
#284=PLANE('',#1500);
#285=PLANE('',#1501);
#325=FACE_OUTER_BOUND('',#408,.T.);
#326=FACE_OUTER_BOUND('',#409,.T.);
#327=FACE_OUTER_BOUND('',#410,.T.);
#328=FACE_OUTER_BOUND('',#411,.T.);
#329=FACE_OUTER_BOUND('',#412,.T.);
#330=FACE_OUTER_BOUND('',#413,.T.);
#331=FACE_OUTER_BOUND('',#414,.T.);
#332=FACE_OUTER_BOUND('',#420,.T.);
#408=EDGE_LOOP('',(#980,#981,#982,#983));
#409=EDGE_LOOP('',(#984,#985,#986,#987));
#410=EDGE_LOOP('',(#988,#989,#990,#991));
#411=EDGE_LOOP('',(#992,#993,#994,#995));
#412=EDGE_LOOP('',(#996,#997,#998,#999));
#413=EDGE_LOOP('',(#1000,#1001,#1002,#1003));
#414=EDGE_LOOP('',(#1004));
#415=EDGE_LOOP('',(#1005));
#416=EDGE_LOOP('',(#1006));
#417=EDGE_LOOP('',(#1007));
#418=EDGE_LOOP('',(#1008));
#419=EDGE_LOOP('',(#1009));
#420=EDGE_LOOP('',(#1010));
#421=EDGE_LOOP('',(#1011));
#422=EDGE_LOOP('',(#1012));
#423=EDGE_LOOP('',(#1013));
#424=EDGE_LOOP('',(#1014));
#425=EDGE_LOOP('',(#1015));
#514=LINE('',#2145,#570);
#515=LINE('',#2151,#571);
#516=LINE('',#2157,#572);
#517=LINE('',#2163,#573);
#518=LINE('',#2169,#574);
#519=LINE('',#2175,#575);
#570=VECTOR('',#1719,0.44);
#571=VECTOR('',#1726,0.44);
#572=VECTOR('',#1733,0.44);
#573=VECTOR('',#1740,0.44);
#574=VECTOR('',#1747,1.065);
#575=VECTOR('',#1754,3.5);
#634=CIRCLE('',#1483,0.44);
#635=CIRCLE('',#1484,0.44);
#636=CIRCLE('',#1486,0.44);
#637=CIRCLE('',#1487,0.44);
#638=CIRCLE('',#1489,0.44);
#639=CIRCLE('',#1490,0.44);
#640=CIRCLE('',#1492,0.44);
#641=CIRCLE('',#1493,0.44);
#642=CIRCLE('',#1495,1.065);
#643=CIRCLE('',#1496,1.065);
#644=CIRCLE('',#1498,3.5);
#645=CIRCLE('',#1499,3.5);
#706=VERTEX_POINT('',#2142);
#707=VERTEX_POINT('',#2144);
#708=VERTEX_POINT('',#2148);
#709=VERTEX_POINT('',#2150);
#710=VERTEX_POINT('',#2154);
#711=VERTEX_POINT('',#2156);
#712=VERTEX_POINT('',#2160);
#713=VERTEX_POINT('',#2162);
#714=VERTEX_POINT('',#2166);
#715=VERTEX_POINT('',#2168);
#716=VERTEX_POINT('',#2172);
#717=VERTEX_POINT('',#2174);
#810=EDGE_CURVE('',#706,#706,#634,.T.);
#811=EDGE_CURVE('',#706,#707,#514,.T.);
#812=EDGE_CURVE('',#707,#707,#635,.T.);
#813=EDGE_CURVE('',#708,#708,#636,.T.);
#814=EDGE_CURVE('',#708,#709,#515,.T.);
#815=EDGE_CURVE('',#709,#709,#637,.T.);
#816=EDGE_CURVE('',#710,#710,#638,.T.);
#817=EDGE_CURVE('',#710,#711,#516,.T.);
#818=EDGE_CURVE('',#711,#711,#639,.T.);
#819=EDGE_CURVE('',#712,#712,#640,.T.);
#820=EDGE_CURVE('',#712,#713,#517,.T.);
#821=EDGE_CURVE('',#713,#713,#641,.T.);
#822=EDGE_CURVE('',#714,#714,#642,.T.);
#823=EDGE_CURVE('',#714,#715,#518,.T.);
#824=EDGE_CURVE('',#715,#715,#643,.T.);
#825=EDGE_CURVE('',#716,#716,#644,.T.);
#826=EDGE_CURVE('',#716,#717,#519,.T.);
#827=EDGE_CURVE('',#717,#717,#645,.T.);
#980=ORIENTED_EDGE('',*,*,#810,.F.);
#981=ORIENTED_EDGE('',*,*,#811,.T.);
#982=ORIENTED_EDGE('',*,*,#812,.F.);
#983=ORIENTED_EDGE('',*,*,#811,.F.);
#984=ORIENTED_EDGE('',*,*,#813,.F.);
#985=ORIENTED_EDGE('',*,*,#814,.T.);
#986=ORIENTED_EDGE('',*,*,#815,.F.);
#987=ORIENTED_EDGE('',*,*,#814,.F.);
#988=ORIENTED_EDGE('',*,*,#816,.F.);
#989=ORIENTED_EDGE('',*,*,#817,.T.);
#990=ORIENTED_EDGE('',*,*,#818,.F.);
#991=ORIENTED_EDGE('',*,*,#817,.F.);
#992=ORIENTED_EDGE('',*,*,#819,.F.);
#993=ORIENTED_EDGE('',*,*,#820,.T.);
#994=ORIENTED_EDGE('',*,*,#821,.F.);
#995=ORIENTED_EDGE('',*,*,#820,.F.);
#996=ORIENTED_EDGE('',*,*,#822,.F.);
#997=ORIENTED_EDGE('',*,*,#823,.T.);
#998=ORIENTED_EDGE('',*,*,#824,.T.);
#999=ORIENTED_EDGE('',*,*,#823,.F.);
#1000=ORIENTED_EDGE('',*,*,#825,.F.);
#1001=ORIENTED_EDGE('',*,*,#826,.T.);
#1002=ORIENTED_EDGE('',*,*,#827,.T.);
#1003=ORIENTED_EDGE('',*,*,#826,.F.);
#1004=ORIENTED_EDGE('',*,*,#825,.T.);
#1005=ORIENTED_EDGE('',*,*,#822,.T.);
#1006=ORIENTED_EDGE('',*,*,#821,.T.);
#1007=ORIENTED_EDGE('',*,*,#818,.T.);
#1008=ORIENTED_EDGE('',*,*,#815,.T.);
#1009=ORIENTED_EDGE('',*,*,#812,.T.);
#1010=ORIENTED_EDGE('',*,*,#827,.F.);
#1011=ORIENTED_EDGE('',*,*,#824,.F.);
#1012=ORIENTED_EDGE('',*,*,#819,.T.);
#1013=ORIENTED_EDGE('',*,*,#816,.T.);
#1014=ORIENTED_EDGE('',*,*,#813,.T.);
#1015=ORIENTED_EDGE('',*,*,#810,.T.);
#1232=CYLINDRICAL_SURFACE('',#1482,0.44);
#1233=CYLINDRICAL_SURFACE('',#1485,0.44);
#1234=CYLINDRICAL_SURFACE('',#1488,0.44);
#1235=CYLINDRICAL_SURFACE('',#1491,0.44);
#1236=CYLINDRICAL_SURFACE('',#1494,1.065);
#1237=CYLINDRICAL_SURFACE('',#1497,3.5);
#1270=ADVANCED_FACE('',(#325),#1232,.F.);
#1271=ADVANCED_FACE('',(#326),#1233,.F.);
#1272=ADVANCED_FACE('',(#327),#1234,.F.);
#1273=ADVANCED_FACE('',(#328),#1235,.F.);
#1274=ADVANCED_FACE('',(#329),#1236,.F.);
#1275=ADVANCED_FACE('',(#330),#1237,.T.);
#1276=ADVANCED_FACE('',(#331,#241,#242,#243,#244,#245),#284,.T.);
#1277=ADVANCED_FACE('',(#332,#246,#247,#248,#249,#250),#285,.F.);
#1331=CLOSED_SHELL('',(#1270,#1271,#1272,#1273,#1274,#1275,#1276,#1277));
#1481=AXIS2_PLACEMENT_3D('',#2140,#1713,#1714);
#1482=AXIS2_PLACEMENT_3D('',#2141,#1715,#1716);
#1483=AXIS2_PLACEMENT_3D('',#2143,#1717,#1718);
#1484=AXIS2_PLACEMENT_3D('',#2146,#1720,#1721);
#1485=AXIS2_PLACEMENT_3D('',#2147,#1722,#1723);
#1486=AXIS2_PLACEMENT_3D('',#2149,#1724,#1725);
#1487=AXIS2_PLACEMENT_3D('',#2152,#1727,#1728);
#1488=AXIS2_PLACEMENT_3D('',#2153,#1729,#1730);
#1489=AXIS2_PLACEMENT_3D('',#2155,#1731,#1732);
#1490=AXIS2_PLACEMENT_3D('',#2158,#1734,#1735);
#1491=AXIS2_PLACEMENT_3D('',#2159,#1736,#1737);
#1492=AXIS2_PLACEMENT_3D('',#2161,#1738,#1739);
#1493=AXIS2_PLACEMENT_3D('',#2164,#1741,#1742);
#1494=AXIS2_PLACEMENT_3D('',#2165,#1743,#1744);
#1495=AXIS2_PLACEMENT_3D('',#2167,#1745,#1746);
#1496=AXIS2_PLACEMENT_3D('',#2170,#1748,#1749);
#1497=AXIS2_PLACEMENT_3D('',#2171,#1750,#1751);
#1498=AXIS2_PLACEMENT_3D('',#2173,#1752,#1753);
#1499=AXIS2_PLACEMENT_3D('',#2176,#1755,#1756);
#1500=AXIS2_PLACEMENT_3D('',#2177,#1757,#1758);
#1501=AXIS2_PLACEMENT_3D('',#2178,#1759,#1760);
#1713=DIRECTION('axis',(0.,0.,1.));
#1714=DIRECTION('refdir',(1.,0.,0.));
#1715=DIRECTION('center_axis',(1.,0.,0.));
#1716=DIRECTION('ref_axis',(0.,0.,-1.));
#1717=DIRECTION('center_axis',(1.,0.,0.));
#1718=DIRECTION('ref_axis',(0.,0.,-1.));
#1719=DIRECTION('',(1.,0.,0.));
#1720=DIRECTION('center_axis',(-1.,0.,0.));
#1721=DIRECTION('ref_axis',(0.,0.,-1.));
#1722=DIRECTION('center_axis',(1.,0.,0.));
#1723=DIRECTION('ref_axis',(0.,0.,-1.));
#1724=DIRECTION('center_axis',(1.,0.,0.));
#1725=DIRECTION('ref_axis',(0.,0.,-1.));
#1726=DIRECTION('',(1.,0.,0.));
#1727=DIRECTION('center_axis',(-1.,0.,0.));
#1728=DIRECTION('ref_axis',(0.,0.,-1.));
#1729=DIRECTION('center_axis',(1.,0.,0.));
#1730=DIRECTION('ref_axis',(0.,0.,-1.));
#1731=DIRECTION('center_axis',(1.,0.,0.));
#1732=DIRECTION('ref_axis',(0.,0.,-1.));
#1733=DIRECTION('',(1.,0.,0.));
#1734=DIRECTION('center_axis',(-1.,0.,0.));
#1735=DIRECTION('ref_axis',(0.,0.,-1.));
#1736=DIRECTION('center_axis',(1.,0.,0.));
#1737=DIRECTION('ref_axis',(0.,0.,-1.));
#1738=DIRECTION('center_axis',(1.,0.,0.));
#1739=DIRECTION('ref_axis',(0.,0.,-1.));
#1740=DIRECTION('',(1.,0.,0.));
#1741=DIRECTION('center_axis',(-1.,0.,0.));
#1742=DIRECTION('ref_axis',(0.,0.,-1.));
#1743=DIRECTION('center_axis',(1.,0.,0.));
#1744=DIRECTION('ref_axis',(0.,0.,-1.));
#1745=DIRECTION('center_axis',(-1.,0.,0.));
#1746=DIRECTION('ref_axis',(0.,0.,-1.));
#1747=DIRECTION('',(-1.,0.,0.));
#1748=DIRECTION('center_axis',(-1.,0.,0.));
#1749=DIRECTION('ref_axis',(0.,0.,-1.));
#1750=DIRECTION('center_axis',(1.,0.,0.));
#1751=DIRECTION('ref_axis',(0.,0.,-1.));
#1752=DIRECTION('center_axis',(1.,0.,0.));
#1753=DIRECTION('ref_axis',(0.,0.,-1.));
#1754=DIRECTION('',(-1.,0.,0.));
#1755=DIRECTION('center_axis',(1.,0.,0.));
#1756=DIRECTION('ref_axis',(0.,0.,-1.));
#1757=DIRECTION('center_axis',(1.,0.,0.));
#1758=DIRECTION('ref_axis',(0.,0.,-1.));
#1759=DIRECTION('center_axis',(1.,0.,0.));
#1760=DIRECTION('ref_axis',(0.,0.,-1.));
#2140=CARTESIAN_POINT('',(0.,0.,0.));
#2141=CARTESIAN_POINT('Origin',(9.1,-1.90918830920368,-1.90918830920368));
#2142=CARTESIAN_POINT('',(9.2,-1.90918830920368,-1.46918830920368));
#2143=CARTESIAN_POINT('Origin',(9.2,-1.90918830920368,-1.90918830920368));
#2144=CARTESIAN_POINT('',(10.,-1.90918830920368,-1.46918830920368));
#2145=CARTESIAN_POINT('',(9.1,-1.90918830920368,-1.46918830920368));
#2146=CARTESIAN_POINT('Origin',(10.,-1.90918830920368,-1.90918830920368));
#2147=CARTESIAN_POINT('Origin',(9.1,-1.90918830920368,1.90918830920368));
#2148=CARTESIAN_POINT('',(9.2,-1.90918830920368,2.34918830920368));
#2149=CARTESIAN_POINT('Origin',(9.2,-1.90918830920368,1.90918830920368));
#2150=CARTESIAN_POINT('',(10.,-1.90918830920368,2.34918830920368));
#2151=CARTESIAN_POINT('',(9.1,-1.90918830920368,2.34918830920368));
#2152=CARTESIAN_POINT('Origin',(10.,-1.90918830920368,1.90918830920368));
#2153=CARTESIAN_POINT('Origin',(9.1,1.90918830920368,1.90918830920368));
#2154=CARTESIAN_POINT('',(9.2,1.90918830920368,2.34918830920368));
#2155=CARTESIAN_POINT('Origin',(9.2,1.90918830920368,1.90918830920368));
#2156=CARTESIAN_POINT('',(10.,1.90918830920368,2.34918830920368));
#2157=CARTESIAN_POINT('',(9.1,1.90918830920368,2.34918830920368));
#2158=CARTESIAN_POINT('Origin',(10.,1.90918830920368,1.90918830920368));
#2159=CARTESIAN_POINT('Origin',(9.1,1.90918830920368,-1.90918830920368));
#2160=CARTESIAN_POINT('',(9.2,1.90918830920368,-1.46918830920368));
#2161=CARTESIAN_POINT('Origin',(9.2,1.90918830920368,-1.90918830920368));
#2162=CARTESIAN_POINT('',(10.,1.90918830920368,-1.46918830920368));
#2163=CARTESIAN_POINT('',(9.1,1.90918830920368,-1.46918830920368));
#2164=CARTESIAN_POINT('Origin',(10.,1.90918830920368,-1.90918830920368));
#2165=CARTESIAN_POINT('Origin',(9.2,0.,0.));
#2166=CARTESIAN_POINT('',(10.,-1.30424884109193E-16,1.065));
#2167=CARTESIAN_POINT('Origin',(10.,0.,0.));
#2168=CARTESIAN_POINT('',(9.2,-1.30424884109193E-16,1.065));
#2169=CARTESIAN_POINT('',(9.2,-1.30424884109193E-16,1.065));
#2170=CARTESIAN_POINT('Origin',(9.2,0.,0.));
#2171=CARTESIAN_POINT('Origin',(9.2,0.,0.));
#2172=CARTESIAN_POINT('',(10.,-4.28626379701574E-16,3.5));
#2173=CARTESIAN_POINT('Origin',(10.,0.,0.));
#2174=CARTESIAN_POINT('',(9.2,-4.28626379701574E-16,3.5));
#2175=CARTESIAN_POINT('',(9.2,-4.28626379701574E-16,3.5));
#2176=CARTESIAN_POINT('Origin',(9.2,0.,0.));
#2177=CARTESIAN_POINT('Origin',(10.,0.,0.));
#2178=CARTESIAN_POINT('Origin',(9.2,0.,0.));
#2487=UNCERTAINTY_MEASURE_WITH_UNIT(LENGTH_MEASURE(0.001),#2508,
'DISTANCE_ACCURACY_VALUE',
'Maximum model space distance between geometric entities at asserted c
onnectivities');
#2495=UNCERTAINTY_MEASURE_WITH_UNIT(LENGTH_MEASURE(0.001),#2508,
'DISTANCE_ACCURACY_VALUE',
'Maximum model space distance between geometric entities at asserted c
onnectivities');
#2499=(
GEOMETRIC_REPRESENTATION_CONTEXT(3)
GLOBAL_UNCERTAINTY_ASSIGNED_CONTEXT((#2487))
GLOBAL_UNIT_ASSIGNED_CONTEXT((#2508,#2510,#2511))
REPRESENTATION_CONTEXT('','3D')
);
#2507=(
GEOMETRIC_REPRESENTATION_CONTEXT(3)
GLOBAL_UNCERTAINTY_ASSIGNED_CONTEXT((#2495))
GLOBAL_UNIT_ASSIGNED_CONTEXT((#2508,#2510,#2511))
REPRESENTATION_CONTEXT('','3D')
);
#2508=(
LENGTH_UNIT()
NAMED_UNIT(*)
SI_UNIT(.CENTI.,.METRE.)
);
#2510=(
NAMED_UNIT(*)
PLANE_ANGLE_UNIT()
SI_UNIT($,.RADIAN.)
);
#2511=(
NAMED_UNIT(*)
SI_UNIT($,.STERADIAN.)
SOLID_ANGLE_UNIT()
);
#2515=SHAPE_DEFINITION_REPRESENTATION(#2526,#2576);
#2526=PRODUCT_DEFINITION_SHAPE('',$,#2588);
#2576=SHAPE_REPRESENTATION('',(#1481),#2499);
#2584=PRODUCT_DEFINITION_CONTEXT('part definition',#2619,'design');
#2588=PRODUCT_DEFINITION('Weld-on flange (1)',
'Weld-on flange (1)',#2599,#2584);
#2599=PRODUCT_DEFINITION_FORMATION('',$,#2624);
#2619=APPLICATION_CONTEXT(
'Core Data for Automotive Mechanical Design Process');
#2620=PRODUCT_CONTEXT('part definition',#2619,'mechanical');
#2624=PRODUCT('Weld-on flange (1)','Weld-on flange (1)',
'Weld-on flange (1)',(#2620));
#2681=COLOUR_RGB('Sky Blue',0.24,0.69,0.87);
#2682=FILL_AREA_STYLE_COLOUR('',#2681);
#2683=FILL_AREA_STYLE('',(#2682));
#2684=SURFACE_STYLE_FILL_AREA(#2683);
#2685=SURFACE_SIDE_STYLE('',(#2684));
#2686=SURFACE_STYLE_USAGE(.BOTH.,#2685);
#2687=PRESENTATION_STYLE_ASSIGNMENT((#2686));
ENDSEC;
END-ISO-10303-21;
